ISO-10303-21;
HEADER;
/* Generated by software containing ST-Developer
 * from STEP Tools, Inc. (www.steptools.com) 
 */

FILE_DESCRIPTION(
/* description */ ('Pallet stop with pneumatic fitting'),
/* implementation_level */ '2;1');

FILE_NAME(
/* name */ 'Cap Screw - M5x20.step',
/* time_stamp */ '2026-10-27T10:51:41-07:00',
/* author */ (''),
/* organization */ (''),
/* preprocessor_version */ 'ST-DEVELOPER v20.2',
/* originating_system */ 'Autodesk Translation Framework v15.17.0.0',
/* authorisation */ '');

FILE_SCHEMA (('AUTOMOTIVE_DESIGN { 1 0 10303 214 3 1 1 }'));
ENDSEC;

DATA;
#10=MECHANICAL_DESIGN_GEOMETRIC_PRESENTATION_REPRESENTATION('',(#377),#10265);
#23=ORIENTED_CLOSED_SHELL('',*,#5066,.F.);
#25=CONICAL_SURFACE('',#5806,0.4,0.785398163397448);
#26=CONICAL_SURFACE('',#5810,0.41,0.785398163397448);
#27=CONICAL_SURFACE('',#5814,0.26,0.463647609000806);
#28=CONICAL_SURFACE('',#5818,0.225,0.785398163397448);
#38=BREP_WITH_VOIDS('Body1',#5065,(#23));
#313=SHAPE_REPRESENTATION_RELATIONSHIP('SRR','None',#10427,#345);
#345=ADVANCED_BREP_SHAPE_REPRESENTATION('',(#38),#10251);
#377=STYLED_ITEM('',(#10662),#38);
#515=FACE_BOUND('',#1334,.T.);
#649=PLANE('',#5804);
#650=PLANE('',#5812);
#651=PLANE('',#5820);
#652=PLANE('',#5821);
#653=PLANE('',#5822);
#654=PLANE('',#5823);
#655=PLANE('',#5824);
#656=PLANE('',#5825);
#657=PLANE('',#5826);
#658=PLANE('',#5827);
#659=PLANE('',#5828);
#919=FACE_OUTER_BOUND('',#1329,.T.);
#920=FACE_OUTER_BOUND('',#1330,.T.);
#921=FACE_OUTER_BOUND('',#1331,.T.);
#922=FACE_OUTER_BOUND('',#1332,.T.);
#923=FACE_OUTER_BOUND('',#1333,.T.);
#924=FACE_OUTER_BOUND('',#1335,.T.);
#925=FACE_OUTER_BOUND('',#1336,.T.);
#926=FACE_OUTER_BOUND('',#1337,.T.);
#927=FACE_OUTER_BOUND('',#1338,.T.);
#928=FACE_OUTER_BOUND('',#1339,.T.);
#929=FACE_OUTER_BOUND('',#1340,.T.);
#930=FACE_OUTER_BOUND('',#1341,.T.);
#931=FACE_OUTER_BOUND('',#1342,.T.);
#932=FACE_OUTER_BOUND('',#1343,.T.);
#933=FACE_OUTER_BOUND('',#1344,.T.);
#934=FACE_OUTER_BOUND('',#1345,.T.);
#935=FACE_OUTER_BOUND('',#1346,.T.);
#1329=EDGE_LOOP('',(#4096));
#1330=EDGE_LOOP('',(#4097,#4098,#4099,#4100));
#1331=EDGE_LOOP('',(#4101,#4102,#4103,#4104));
#1332=EDGE_LOOP('',(#4105,#4106,#4107,#4108));
#1333=EDGE_LOOP('',(#4109));
#1334=EDGE_LOOP('',(#4110));
#1335=EDGE_LOOP('',(#4111,#4112,#4113,#4114));
#1336=EDGE_LOOP('',(#4115,#4116,#4117,#4118));
#1337=EDGE_LOOP('',(#4119,#4120,#4121,#4122));
#1338=EDGE_LOOP('',(#4123));
#1339=EDGE_LOOP('',(#4124,#4125,#4126,#4127));
#1340=EDGE_LOOP('',(#4128,#4129,#4130,#4131));
#1341=EDGE_LOOP('',(#4132,#4133,#4134,#4135));
#1342=EDGE_LOOP('',(#4136,#4137,#4138,#4139));
#1343=EDGE_LOOP('',(#4140,#4141,#4142,#4143));
#1344=EDGE_LOOP('',(#4144,#4145,#4146,#4147));
#1345=EDGE_LOOP('',(#4148,#4149,#4150,#4151,#4152,#4153));
#1346=EDGE_LOOP('',(#4154,#4155,#4156,#4157,#4158,#4159));
#1662=LINE('',#9476,#1997);
#1663=LINE('',#9480,#1998);
#1664=LINE('',#9484,#1999);
#1665=LINE('',#9491,#2000);
#1666=LINE('',#9495,#2001);
#1667=LINE('',#9499,#2002);
#1668=LINE('',#9504,#2003);
#1669=LINE('',#9506,#2004);
#1670=LINE('',#9508,#2005);
#1671=LINE('',#9509,#2006);
#1672=LINE('',#9512,#2007);
#1673=LINE('',#9514,#2008);
#1674=LINE('',#9515,#2009);
#1675=LINE('',#9518,#2010);
#1676=LINE('',#9520,#2011);
#1677=LINE('',#9521,#2012);
#1678=LINE('',#9524,#2013);
#1679=LINE('',#9526,#2014);
#1680=LINE('',#9527,#2015);
#1681=LINE('',#9530,#2016);
#1682=LINE('',#9532,#2017);
#1683=LINE('',#9533,#2018);
#1684=LINE('',#9535,#2019);
#1685=LINE('',#9536,#2020);
#1997=VECTOR('',#7013,0.4);
#1998=VECTOR('',#7018,0.425);
#1999=VECTOR('',#7023,0.41);
#2000=VECTOR('',#7032,0.26);
#2001=VECTOR('',#7037,0.25);
#2002=VECTOR('',#7042,0.225);
#2003=VECTOR('',#7047,1.);
#2004=VECTOR('',#7048,1.);
#2005=VECTOR('',#7049,1.);
#2006=VECTOR('',#7050,1.);
#2007=VECTOR('',#7053,1.);
#2008=VECTOR('',#7054,1.);
#2009=VECTOR('',#7055,1.);
#2010=VECTOR('',#7058,1.);
#2011=VECTOR('',#7059,1.);
#2012=VECTOR('',#7060,1.);
#2013=VECTOR('',#7063,1.);
#2014=VECTOR('',#7064,1.);
#2015=VECTOR('',#7065,1.);
#2016=VECTOR('',#7068,1.);
#2017=VECTOR('',#7069,1.);
#2018=VECTOR('',#7070,1.);
#2019=VECTOR('',#7073,1.);
#2020=VECTOR('',#7074,1.);
#2324=CIRCLE('',#5805,0.375);
#2325=CIRCLE('',#5807,0.425);
#2326=CIRCLE('',#5809,0.425);
#2327=CIRCLE('',#5811,0.395);
#2328=CIRCLE('',#5813,0.27);
#2329=CIRCLE('',#5815,0.24505);
#2330=CIRCLE('',#5817,0.24505);
#2331=CIRCLE('',#5819,0.2);
#2634=VERTEX_POINT('',#9471);
#2635=VERTEX_POINT('',#9474);
#2636=VERTEX_POINT('',#9478);
#2637=VERTEX_POINT('',#9482);
#2638=VERTEX_POINT('',#9486);
#2639=VERTEX_POINT('',#9489);
#2640=VERTEX_POINT('',#9493);
#2641=VERTEX_POINT('',#9497);
#2642=VERTEX_POINT('',#9502);
#2643=VERTEX_POINT('',#9503);
#2644=VERTEX_POINT('',#9505);
#2645=VERTEX_POINT('',#9507);
#2646=VERTEX_POINT('',#9511);
#2647=VERTEX_POINT('',#9513);
#2648=VERTEX_POINT('',#9517);
#2649=VERTEX_POINT('',#9519);
#2650=VERTEX_POINT('',#9523);
#2651=VERTEX_POINT('',#9525);
#2652=VERTEX_POINT('',#9529);
#2653=VERTEX_POINT('',#9531);
#3147=EDGE_CURVE('',#2634,#2634,#2324,.T.);
#3148=EDGE_CURVE('',#2635,#2635,#2325,.T.);
#3149=EDGE_CURVE('',#2635,#2634,#1662,.T.);
#3150=EDGE_CURVE('',#2636,#2636,#2326,.T.);
#3151=EDGE_CURVE('',#2636,#2635,#1663,.T.);
#3152=EDGE_CURVE('',#2637,#2637,#2327,.T.);
#3153=EDGE_CURVE('',#2637,#2636,#1664,.T.);
#3154=EDGE_CURVE('',#2638,#2638,#2328,.T.);
#3155=EDGE_CURVE('',#2639,#2639,#2329,.F.);
#3156=EDGE_CURVE('',#2639,#2638,#1665,.T.);
#3157=EDGE_CURVE('',#2640,#2640,#2330,.F.);
#3158=EDGE_CURVE('',#2640,#2639,#1666,.T.);
#3159=EDGE_CURVE('',#2641,#2641,#2331,.T.);
#3160=EDGE_CURVE('',#2641,#2640,#1667,.T.);
#3161=EDGE_CURVE('',#2642,#2643,#1668,.T.);
#3162=EDGE_CURVE('',#2643,#2644,#1669,.T.);
#3163=EDGE_CURVE('',#2644,#2645,#1670,.T.);
#3164=EDGE_CURVE('',#2642,#2645,#1671,.T.);
#3165=EDGE_CURVE('',#2643,#2646,#1672,.T.);
#3166=EDGE_CURVE('',#2646,#2647,#1673,.T.);
#3167=EDGE_CURVE('',#2647,#2644,#1674,.T.);
#3168=EDGE_CURVE('',#2646,#2648,#1675,.T.);
#3169=EDGE_CURVE('',#2648,#2649,#1676,.T.);
#3170=EDGE_CURVE('',#2649,#2647,#1677,.T.);
#3171=EDGE_CURVE('',#2648,#2650,#1678,.T.);
#3172=EDGE_CURVE('',#2650,#2651,#1679,.T.);
#3173=EDGE_CURVE('',#2651,#2649,#1680,.T.);
#3174=EDGE_CURVE('',#2650,#2652,#1681,.T.);
#3175=EDGE_CURVE('',#2652,#2653,#1682,.T.);
#3176=EDGE_CURVE('',#2653,#2651,#1683,.T.);
#3177=EDGE_CURVE('',#2652,#2642,#1684,.T.);
#3178=EDGE_CURVE('',#2645,#2653,#1685,.T.);
#4096=ORIENTED_EDGE('',*,*,#3147,.F.);
#4097=ORIENTED_EDGE('',*,*,#3148,.F.);
#4098=ORIENTED_EDGE('',*,*,#3149,.T.);
#4099=ORIENTED_EDGE('',*,*,#3147,.T.);
#4100=ORIENTED_EDGE('',*,*,#3149,.F.);
#4101=ORIENTED_EDGE('',*,*,#3150,.F.);
#4102=ORIENTED_EDGE('',*,*,#3151,.T.);
#4103=ORIENTED_EDGE('',*,*,#3148,.T.);
#4104=ORIENTED_EDGE('',*,*,#3151,.F.);
#4105=ORIENTED_EDGE('',*,*,#3152,.F.);
#4106=ORIENTED_EDGE('',*,*,#3153,.T.);
#4107=ORIENTED_EDGE('',*,*,#3150,.T.);
#4108=ORIENTED_EDGE('',*,*,#3153,.F.);
#4109=ORIENTED_EDGE('',*,*,#3152,.T.);
#4110=ORIENTED_EDGE('',*,*,#3154,.F.);
#4111=ORIENTED_EDGE('',*,*,#3155,.F.);
#4112=ORIENTED_EDGE('',*,*,#3156,.T.);
#4113=ORIENTED_EDGE('',*,*,#3154,.T.);
#4114=ORIENTED_EDGE('',*,*,#3156,.F.);
#4115=ORIENTED_EDGE('',*,*,#3157,.F.);
#4116=ORIENTED_EDGE('',*,*,#3158,.T.);
#4117=ORIENTED_EDGE('',*,*,#3155,.T.);
#4118=ORIENTED_EDGE('',*,*,#3158,.F.);
#4119=ORIENTED_EDGE('',*,*,#3159,.F.);
#4120=ORIENTED_EDGE('',*,*,#3160,.T.);
#4121=ORIENTED_EDGE('',*,*,#3157,.T.);
#4122=ORIENTED_EDGE('',*,*,#3160,.F.);
#4123=ORIENTED_EDGE('',*,*,#3159,.T.);
#4124=ORIENTED_EDGE('',*,*,#3161,.T.);
#4125=ORIENTED_EDGE('',*,*,#3162,.T.);
#4126=ORIENTED_EDGE('',*,*,#3163,.T.);
#4127=ORIENTED_EDGE('',*,*,#3164,.F.);
#4128=ORIENTED_EDGE('',*,*,#3165,.T.);
#4129=ORIENTED_EDGE('',*,*,#3166,.T.);
#4130=ORIENTED_EDGE('',*,*,#3167,.T.);
#4131=ORIENTED_EDGE('',*,*,#3162,.F.);
#4132=ORIENTED_EDGE('',*,*,#3168,.T.);
#4133=ORIENTED_EDGE('',*,*,#3169,.T.);
#4134=ORIENTED_EDGE('',*,*,#3170,.T.);
#4135=ORIENTED_EDGE('',*,*,#3166,.F.);
#4136=ORIENTED_EDGE('',*,*,#3171,.T.);
#4137=ORIENTED_EDGE('',*,*,#3172,.T.);
#4138=ORIENTED_EDGE('',*,*,#3173,.T.);
#4139=ORIENTED_EDGE('',*,*,#3169,.F.);
#4140=ORIENTED_EDGE('',*,*,#3174,.T.);
#4141=ORIENTED_EDGE('',*,*,#3175,.T.);
#4142=ORIENTED_EDGE('',*,*,#3176,.T.);
#4143=ORIENTED_EDGE('',*,*,#3172,.F.);
#4144=ORIENTED_EDGE('',*,*,#3177,.T.);
#4145=ORIENTED_EDGE('',*,*,#3164,.T.);
#4146=ORIENTED_EDGE('',*,*,#3178,.T.);
#4147=ORIENTED_EDGE('',*,*,#3175,.F.);
#4148=ORIENTED_EDGE('',*,*,#3177,.F.);
#4149=ORIENTED_EDGE('',*,*,#3174,.F.);
#4150=ORIENTED_EDGE('',*,*,#3171,.F.);
#4151=ORIENTED_EDGE('',*,*,#3168,.F.);
#4152=ORIENTED_EDGE('',*,*,#3165,.F.);
#4153=ORIENTED_EDGE('',*,*,#3161,.F.);
#4154=ORIENTED_EDGE('',*,*,#3178,.F.);
#4155=ORIENTED_EDGE('',*,*,#3163,.F.);
#4156=ORIENTED_EDGE('',*,*,#3167,.F.);
#4157=ORIENTED_EDGE('',*,*,#3170,.F.);
#4158=ORIENTED_EDGE('',*,*,#3173,.F.);
#4159=ORIENTED_EDGE('',*,*,#3176,.F.);
#4700=CYLINDRICAL_SURFACE('',#5808,0.425);
#4701=CYLINDRICAL_SURFACE('',#5816,0.24505);
#4914=ADVANCED_FACE('',(#919),#649,.T.);
#4915=ADVANCED_FACE('',(#920),#25,.T.);
#4916=ADVANCED_FACE('',(#921),#4700,.T.);
#4917=ADVANCED_FACE('',(#922),#26,.T.);
#4918=ADVANCED_FACE('',(#923,#515),#650,.T.);
#4919=ADVANCED_FACE('',(#924),#27,.T.);
#4920=ADVANCED_FACE('',(#925),#4701,.T.);
#4921=ADVANCED_FACE('',(#926),#28,.T.);
#4922=ADVANCED_FACE('',(#927),#651,.T.);
#4923=ADVANCED_FACE('',(#928),#652,.F.);
#4924=ADVANCED_FACE('',(#929),#653,.F.);
#4925=ADVANCED_FACE('',(#930),#654,.F.);
#4926=ADVANCED_FACE('',(#931),#655,.F.);
#4927=ADVANCED_FACE('',(#932),#656,.F.);
#4928=ADVANCED_FACE('',(#933),#657,.F.);
#4929=ADVANCED_FACE('',(#934),#658,.F.);
#4930=ADVANCED_FACE('',(#935),#659,.F.);
#5065=CLOSED_SHELL('',(#4914,#4915,#4916,#4917,#4918,#4919,#4920,#4921,
#4922));
#5066=CLOSED_SHELL('',(#4923,#4924,#4925,#4926,#4927,#4928,#4929,#4930));
#5803=AXIS2_PLACEMENT_3D('',#9469,#7003,#7004);
#5804=AXIS2_PLACEMENT_3D('',#9470,#7005,#7006);
#5805=AXIS2_PLACEMENT_3D('',#9472,#7007,#7008);
#5806=AXIS2_PLACEMENT_3D('',#9473,#7009,#7010);
#5807=AXIS2_PLACEMENT_3D('',#9475,#7011,#7012);
#5808=AXIS2_PLACEMENT_3D('',#9477,#7014,#7015);
#5809=AXIS2_PLACEMENT_3D('',#9479,#7016,#7017);
#5810=AXIS2_PLACEMENT_3D('',#9481,#7019,#7020);
#5811=AXIS2_PLACEMENT_3D('',#9483,#7021,#7022);
#5812=AXIS2_PLACEMENT_3D('',#9485,#7024,#7025);
#5813=AXIS2_PLACEMENT_3D('',#9487,#7026,#7027);
#5814=AXIS2_PLACEMENT_3D('',#9488,#7028,#7029);
#5815=AXIS2_PLACEMENT_3D('',#9490,#7030,#7031);
#5816=AXIS2_PLACEMENT_3D('',#9492,#7033,#7034);
#5817=AXIS2_PLACEMENT_3D('',#9494,#7035,#7036);
#5818=AXIS2_PLACEMENT_3D('',#9496,#7038,#7039);
#5819=AXIS2_PLACEMENT_3D('',#9498,#7040,#7041);
#5820=AXIS2_PLACEMENT_3D('',#9500,#7043,#7044);
#5821=AXIS2_PLACEMENT_3D('',#9501,#7045,#7046);
#5822=AXIS2_PLACEMENT_3D('',#9510,#7051,#7052);
#5823=AXIS2_PLACEMENT_3D('',#9516,#7056,#7057);
#5824=AXIS2_PLACEMENT_3D('',#9522,#7061,#7062);
#5825=AXIS2_PLACEMENT_3D('',#9528,#7066,#7067);
#5826=AXIS2_PLACEMENT_3D('',#9534,#7071,#7072);
#5827=AXIS2_PLACEMENT_3D('',#9537,#7075,#7076);
#5828=AXIS2_PLACEMENT_3D('',#9538,#7077,#7078);
#7003=DIRECTION('axis',(0.,0.,1.));
#7004=DIRECTION('refdir',(1.,0.,0.));
#7005=DIRECTION('center_axis',(0.,1.,0.));
#7006=DIRECTION('ref_axis',(0.,0.,1.));
#7007=DIRECTION('center_axis',(0.,-1.,0.));
#7008=DIRECTION('ref_axis',(1.,0.,0.));
#7009=DIRECTION('center_axis',(0.,-1.,0.));
#7010=DIRECTION('ref_axis',(1.,0.,0.));
#7011=DIRECTION('center_axis',(0.,-1.,0.));
#7012=DIRECTION('ref_axis',(1.,0.,0.));
#7013=DIRECTION('',(0.707106781186548,0.707106781186547,8.65956056235493E-17));
#7014=DIRECTION('center_axis',(0.,-1.,0.));
#7015=DIRECTION('ref_axis',(1.,0.,0.));
#7016=DIRECTION('center_axis',(0.,-1.,0.));
#7017=DIRECTION('ref_axis',(1.,0.,0.));
#7018=DIRECTION('',(0.,1.,0.));
#7019=DIRECTION('center_axis',(0.,1.,0.));
#7020=DIRECTION('ref_axis',(1.,0.,0.));
#7021=DIRECTION('center_axis',(0.,-1.,0.));
#7022=DIRECTION('ref_axis',(1.,0.,0.));
#7023=DIRECTION('',(-0.707106781186547,0.707106781186548,-8.65956056235493E-17));
#7024=DIRECTION('center_axis',(0.,-1.,0.));
#7025=DIRECTION('ref_axis',(0.,0.,-1.));
#7026=DIRECTION('center_axis',(0.,-1.,0.));
#7027=DIRECTION('ref_axis',(1.,0.,0.));
#7028=DIRECTION('center_axis',(0.,1.,0.));
#7029=DIRECTION('ref_axis',(1.,0.,0.));
#7030=DIRECTION('center_axis',(0.,1.,0.));
#7031=DIRECTION('ref_axis',(1.,0.,0.));
#7032=DIRECTION('',(-0.447213595499958,0.894427190999916,-5.47678698264203E-17));
#7033=DIRECTION('center_axis',(0.,-1.,0.));
#7034=DIRECTION('ref_axis',(1.,0.,0.));
#7035=DIRECTION('center_axis',(0.,1.,0.));
#7036=DIRECTION('ref_axis',(1.,0.,0.));
#7037=DIRECTION('',(0.,1.,0.));
#7038=DIRECTION('center_axis',(0.,1.,0.));
#7039=DIRECTION('ref_axis',(1.,0.,0.));
#7040=DIRECTION('center_axis',(0.,-1.,0.));
#7041=DIRECTION('ref_axis',(1.,0.,0.));
#7042=DIRECTION('',(-0.707106781186547,0.707106781186548,-8.65956056235493E-17));
#7043=DIRECTION('center_axis',(0.,-1.,0.));
#7044=DIRECTION('ref_axis',(0.,0.,-1.));
#7045=DIRECTION('center_axis',(0.866025403784439,0.,-0.5));
#7046=DIRECTION('ref_axis',(0.5,0.,0.866025403784439));
#7047=DIRECTION('',(-0.5,0.,-0.866025403784439));
#7048=DIRECTION('',(0.,-1.,0.));
#7049=DIRECTION('',(0.5,0.,0.866025403784439));
#7050=DIRECTION('',(0.,-1.,0.));
#7051=DIRECTION('center_axis',(1.20185167898973E-16,0.,-1.));
#7052=DIRECTION('ref_axis',(1.,0.,1.20185167898973E-16));
#7053=DIRECTION('',(-1.,0.,-1.20185167898973E-16));
#7054=DIRECTION('',(0.,-1.,0.));
#7055=DIRECTION('',(1.,0.,1.20185167898973E-16));
#7056=DIRECTION('center_axis',(-0.866025403784439,0.,-0.5));
#7057=DIRECTION('ref_axis',(0.5,0.,-0.866025403784439));
#7058=DIRECTION('',(-0.5,0.,0.866025403784439));
#7059=DIRECTION('',(0.,-1.,0.));
#7060=DIRECTION('',(0.5,0.,-0.866025403784439));
#7061=DIRECTION('center_axis',(-0.866025403784439,0.,0.5));
#7062=DIRECTION('ref_axis',(-0.5,0.,-0.866025403784439));
#7063=DIRECTION('',(0.5,0.,0.866025403784439));
#7064=DIRECTION('',(0.,-1.,0.));
#7065=DIRECTION('',(-0.5,0.,-0.866025403784439));
#7066=DIRECTION('center_axis',(-2.40370335797945E-16,0.,1.));
#7067=DIRECTION('ref_axis',(-1.,0.,-2.40370335797945E-16));
#7068=DIRECTION('',(1.,0.,2.40370335797945E-16));
#7069=DIRECTION('',(0.,-1.,0.));
#7070=DIRECTION('',(-1.,0.,-2.40370335797945E-16));
#7071=DIRECTION('center_axis',(0.866025403784439,0.,0.5));
#7072=DIRECTION('ref_axis',(-0.5,0.,0.866025403784439));
#7073=DIRECTION('',(0.5,0.,-0.866025403784439));
#7074=DIRECTION('',(-0.5,0.,0.866025403784439));
#7075=DIRECTION('center_axis',(0.,1.,0.));
#7076=DIRECTION('ref_axis',(1.,0.,0.));
#7077=DIRECTION('center_axis',(0.,-1.,0.));
#7078=DIRECTION('ref_axis',(0.,0.,-1.));
#9469=CARTESIAN_POINT('',(0.,0.,0.));
#9470=CARTESIAN_POINT('Origin',(0.375,0.5,0.));
#9471=CARTESIAN_POINT('',(-0.375,0.5,-4.59242549680257E-17));
#9472=CARTESIAN_POINT('Origin',(0.,0.5,0.));
#9473=CARTESIAN_POINT('Origin',(0.,0.475,0.));
#9474=CARTESIAN_POINT('',(-0.425,0.45,-5.20474889637625E-17));
#9475=CARTESIAN_POINT('Origin',(0.,0.45,0.));
#9476=CARTESIAN_POINT('',(-0.4,0.475,-4.89858719658941E-17));
#9477=CARTESIAN_POINT('Origin',(0.,0.24,0.));
#9478=CARTESIAN_POINT('',(-0.425,0.0299999999999998,-5.20474889637625E-17));
#9479=CARTESIAN_POINT('Origin',(0.,0.0299999999999998,0.));
#9480=CARTESIAN_POINT('',(-0.425,0.24,-5.20474889637625E-17));
#9481=CARTESIAN_POINT('Origin',(0.,0.0150000000000001,0.));
#9482=CARTESIAN_POINT('',(-0.395,4.85722573273506E-17,-4.83735485663204E-17));
#9483=CARTESIAN_POINT('Origin',(0.,0.,0.));
#9484=CARTESIAN_POINT('',(-0.41,0.0150000000000001,-5.02105187650415E-17));
#9485=CARTESIAN_POINT('Origin',(0.27,0.,0.));
#9486=CARTESIAN_POINT('',(-0.27,0.,-3.30654635769785E-17));
#9487=CARTESIAN_POINT('Origin',(0.,0.,0.));
#9488=CARTESIAN_POINT('Origin',(0.,-0.02,0.));
#9489=CARTESIAN_POINT('',(-0.24505,-0.0498999999999999,3.00099698131059E-17));
#9490=CARTESIAN_POINT('Origin',(0.,-0.0498999999999999,0.));
#9491=CARTESIAN_POINT('',(-0.26,-0.02,-3.18408167778312E-17));
#9492=CARTESIAN_POINT('Origin',(0.,-0.995,0.));
#9493=CARTESIAN_POINT('',(-0.24505,-1.95495,3.00099698131059E-17));
#9494=CARTESIAN_POINT('Origin',(0.,-1.95495,0.));
#9495=CARTESIAN_POINT('',(-0.24505,-0.995,-3.00099698131059E-17));
#9496=CARTESIAN_POINT('Origin',(0.,-1.975,0.));
#9497=CARTESIAN_POINT('',(-0.2,-2.,-2.44929359829471E-17));
#9498=CARTESIAN_POINT('Origin',(0.,-2.,0.));
#9499=CARTESIAN_POINT('',(-0.225,-1.975,-2.75545529808154E-17));
#9500=CARTESIAN_POINT('Origin',(0.,-2.,0.));
#9501=CARTESIAN_POINT('Origin',(0.115470053837925,-0.5,-0.2));
#9502=CARTESIAN_POINT('',(0.23094010767585,-0.5,0.));
#9503=CARTESIAN_POINT('',(0.115470053837925,-0.5,-0.2));
#9504=CARTESIAN_POINT('',(0.23094010767585,-0.5,0.));
#9505=CARTESIAN_POINT('',(0.115470053837925,-0.8,-0.2));
#9506=CARTESIAN_POINT('',(0.115470053837925,-0.5,-0.2));
#9507=CARTESIAN_POINT('',(0.23094010767585,-0.8,0.));
#9508=CARTESIAN_POINT('',(0.23094010767585,-0.8,0.));
#9509=CARTESIAN_POINT('',(0.23094010767585,-0.5,0.));
#9510=CARTESIAN_POINT('Origin',(-0.115470053837925,-0.5,-0.2));
#9511=CARTESIAN_POINT('',(-0.115470053837925,-0.5,-0.2));
#9512=CARTESIAN_POINT('',(0.115470053837925,-0.5,-0.2));
#9513=CARTESIAN_POINT('',(-0.115470053837925,-0.8,-0.2));
#9514=CARTESIAN_POINT('',(-0.115470053837925,-0.5,-0.2));
#9515=CARTESIAN_POINT('',(0.115470053837925,-0.8,-0.2));
#9516=CARTESIAN_POINT('Origin',(-0.23094010767585,-0.5,-2.77555756156289E-17));
#9517=CARTESIAN_POINT('',(-0.23094010767585,-0.5,-2.82820063659975E-17));
#9518=CARTESIAN_POINT('',(-0.115470053837925,-0.5,-0.2));
#9519=CARTESIAN_POINT('',(-0.23094010767585,-0.8,-2.77555756156289E-17));
#9520=CARTESIAN_POINT('',(-0.23094010767585,-0.5,-2.82820063659975E-17));
#9521=CARTESIAN_POINT('',(-0.115470053837925,-0.8,-0.2));
#9522=CARTESIAN_POINT('Origin',(-0.115470053837925,-0.5,0.2));
#9523=CARTESIAN_POINT('',(-0.115470053837925,-0.5,0.2));
#9524=CARTESIAN_POINT('',(-0.23094010767585,-0.5,-2.82820063659975E-17));
#9525=CARTESIAN_POINT('',(-0.115470053837925,-0.8,0.2));
#9526=CARTESIAN_POINT('',(-0.115470053837925,-0.5,0.2));
#9527=CARTESIAN_POINT('',(-0.23094010767585,-0.8,-2.82820063659975E-17));
#9528=CARTESIAN_POINT('Origin',(0.115470053837925,-0.5,0.2));
#9529=CARTESIAN_POINT('',(0.115470053837925,-0.5,0.2));
#9530=CARTESIAN_POINT('',(-0.115470053837925,-0.5,0.2));
#9531=CARTESIAN_POINT('',(0.115470053837925,-0.8,0.2));
#9532=CARTESIAN_POINT('',(0.115470053837925,-0.5,0.2));
#9533=CARTESIAN_POINT('',(-0.115470053837925,-0.8,0.2));
#9534=CARTESIAN_POINT('Origin',(0.23094010767585,-0.5,0.));
#9535=CARTESIAN_POINT('',(0.115470053837925,-0.5,0.2));
#9536=CARTESIAN_POINT('',(0.115470053837925,-0.8,0.2));
#9537=CARTESIAN_POINT('Origin',(0.,-0.5,0.));
#9538=CARTESIAN_POINT('Origin',(0.,-0.8,0.));
#10213=UNCERTAINTY_MEASURE_WITH_UNIT(LENGTH_MEASURE(0.001),#10266,
'DISTANCE_ACCURACY_VALUE',
'Maximum model space distance between geometric entities at asserted c
onnectivities');
#10227=UNCERTAINTY_MEASURE_WITH_UNIT(LENGTH_MEASURE(0.001),#10266,
'DISTANCE_ACCURACY_VALUE',
'Maximum model space distance between geometric entities at asserted c
onnectivities');
#10251=(
GEOMETRIC_REPRESENTATION_CONTEXT(3)
GLOBAL_UNCERTAINTY_ASSIGNED_CONTEXT((#10213))
GLOBAL_UNIT_ASSIGNED_CONTEXT((#10266,#10268,#10269))
REPRESENTATION_CONTEXT('','3D')
);
#10265=(
GEOMETRIC_REPRESENTATION_CONTEXT(3)
GLOBAL_UNCERTAINTY_ASSIGNED_CONTEXT((#10227))
GLOBAL_UNIT_ASSIGNED_CONTEXT((#10266,#10268,#10269))
REPRESENTATION_CONTEXT('','3D')
);
#10266=(
LENGTH_UNIT()
NAMED_UNIT(*)
SI_UNIT(.CENTI.,.METRE.)
);
#10268=(
NAMED_UNIT(*)
PLANE_ANGLE_UNIT()
SI_UNIT($,.RADIAN.)
);
#10269=(
NAMED_UNIT(*)
SI_UNIT($,.STERADIAN.)
SOLID_ANGLE_UNIT()
);
#10293=SHAPE_DEFINITION_REPRESENTATION(#10332,#10427);
#10332=PRODUCT_DEFINITION_SHAPE('',$,#10465);
#10427=SHAPE_REPRESENTATION('',(#5803),#10251);
#10441=PRODUCT_DEFINITION_CONTEXT('part definition',#10554,'design');
#10465=PRODUCT_DEFINITION('Cap Screw - M5x20','Cap Screw - M5x20',#10502,
#10441);
#10502=PRODUCT_DEFINITION_FORMATION('',$,#10579);
#10554=APPLICATION_CONTEXT(
'Core Data for Automotive Mechanical Design Process');
#10555=PRODUCT_CONTEXT('part definition',#10554,'mechanical');
#10579=PRODUCT('Cap Screw - M5x20','Cap Screw - M5x20',
'Cap Screw - M5x20',(#10555));
#10656=COLOUR_RGB('Black',0.12,0.14,0.17);
#10657=FILL_AREA_STYLE_COLOUR('',#10656);
#10658=FILL_AREA_STYLE('',(#10657));
#10659=SURFACE_STYLE_FILL_AREA(#10658);
#10660=SURFACE_SIDE_STYLE('',(#10659));
#10661=SURFACE_STYLE_USAGE(.BOTH.,#10660);
#10662=PRESENTATION_STYLE_ASSIGNMENT((#10661));
ENDSEC;
END-ISO-10303-21;
